ISO-10303-21;
HEADER;
/* Generated by software containing ST-Developer
 * from STEP Tools, Inc. (www.steptools.com) 
 */

FILE_DESCRIPTION(
/* description */ ('Two-stage gear reducer in split housing'),
/* implementation_level */ '2;1');

FILE_NAME(
/* name */ 'M6x18 mounting screw.step',
/* time_stamp */ '2026-10-28T03:22:31-07:00',
/* author */ (''),
/* organization */ (''),
/* preprocessor_version */ 'ST-DEVELOPER v20.2',
/* originating_system */ 'Autodesk Translation Framework v15.17.0.0',
/* authorisation */ '');

FILE_SCHEMA (('AUTOMOTIVE_DESIGN { 1 0 10303 214 3 1 1 }'));
ENDSEC;

DATA;
#10=MECHANICAL_DESIGN_GEOMETRIC_PRESENTATION_REPRESENTATION('',(#1250),#73366);
#1101=CONICAL_SURFACE('',#17405,0.475,0.785398163397449);
#1102=CONICAL_SURFACE('',#17409,0.485,0.785398163397448);
#1103=CONICAL_SURFACE('',#17413,0.31,0.463647609000806);
#1118=ORIENTED_CLOSED_SHELL('',*,#16138,.F.);
#1120=BREP_WITH_VOIDS('Body1',#16139,(#1118));
#1138=SHAPE_REPRESENTATION_RELATIONSHIP('SRR','None',#73625,#1194);
#1194=ADVANCED_BREP_SHAPE_REPRESENTATION('',(#1120),#73321);
#1250=STYLED_ITEM('',(#73995),#1120);
#1518=FACE_BOUND('',#3355,.T.);
#1744=PLANE('',#17393);
#1745=PLANE('',#17394);
#1746=PLANE('',#17395);
#1747=PLANE('',#17396);
#1748=PLANE('',#17397);
#1749=PLANE('',#17398);
#1750=PLANE('',#17399);
#1751=PLANE('',#17400);
#1752=PLANE('',#17401);
#1753=PLANE('',#17403);
#1754=PLANE('',#17411);
#2284=FACE_OUTER_BOUND('',#3341,.T.);
#2285=FACE_OUTER_BOUND('',#3342,.T.);
#2286=FACE_OUTER_BOUND('',#3343,.T.);
#2287=FACE_OUTER_BOUND('',#3344,.T.);
#2288=FACE_OUTER_BOUND('',#3345,.T.);
#2289=FACE_OUTER_BOUND('',#3346,.T.);
#2290=FACE_OUTER_BOUND('',#3347,.T.);
#2291=FACE_OUTER_BOUND('',#3348,.T.);
#2292=FACE_OUTER_BOUND('',#3349,.T.);
#2293=FACE_OUTER_BOUND('',#3350,.T.);
#2294=FACE_OUTER_BOUND('',#3351,.T.);
#2295=FACE_OUTER_BOUND('',#3352,.T.);
#2296=FACE_OUTER_BOUND('',#3353,.T.);
#2297=FACE_OUTER_BOUND('',#3354,.T.);
#2298=FACE_OUTER_BOUND('',#3356,.T.);
#2299=FACE_OUTER_BOUND('',#3357,.T.);
#3341=EDGE_LOOP('',(#11755,#11756,#11757,#11758));
#3342=EDGE_LOOP('',(#11759,#11760,#11761,#11762));
#3343=EDGE_LOOP('',(#11763,#11764,#11765,#11766));
#3344=EDGE_LOOP('',(#11767,#11768,#11769,#11770));
#3345=EDGE_LOOP('',(#11771,#11772,#11773,#11774));
#3346=EDGE_LOOP('',(#11775,#11776,#11777,#11778));
#3347=EDGE_LOOP('',(#11779,#11780,#11781,#11782,#11783,#11784));
#3348=EDGE_LOOP('',(#11785,#11786,#11787,#11788,#11789,#11790));
#3349=EDGE_LOOP('',(#11791));
#3350=EDGE_LOOP('',(#11792));
#3351=EDGE_LOOP('',(#11793,#11794,#11795,#11796));
#3352=EDGE_LOOP('',(#11797,#11798,#11799,#11800));
#3353=EDGE_LOOP('',(#11801,#11802,#11803,#11804));
#3354=EDGE_LOOP('',(#11805));
#3355=EDGE_LOOP('',(#11806));
#3356=EDGE_LOOP('',(#11807,#11808,#11809,#11810));
#3357=EDGE_LOOP('',(#11811,#11812,#11813,#11814));
#4400=LINE('',#24118,#5424);
#4401=LINE('',#24120,#5425);
#4402=LINE('',#24122,#5426);
#4403=LINE('',#24123,#5427);
#4404=LINE('',#24126,#5428);
#4405=LINE('',#24128,#5429);
#4406=LINE('',#24129,#5430);
#4407=LINE('',#24132,#5431);
#4408=LINE('',#24134,#5432);
#4409=LINE('',#24135,#5433);
#4410=LINE('',#24138,#5434);
#4411=LINE('',#24140,#5435);
#4412=LINE('',#24141,#5436);
#4413=LINE('',#24144,#5437);
#4414=LINE('',#24146,#5438);
#4415=LINE('',#24147,#5439);
#4416=LINE('',#24149,#5440);
#4417=LINE('',#24150,#5441);
#4418=LINE('',#24162,#5442);
#4419=LINE('',#24166,#5443);
#4420=LINE('',#24170,#5444);
#4421=LINE('',#24177,#5445);
#4422=LINE('',#24179,#5446);
#5424=VECTOR('',#19966,1.);
#5425=VECTOR('',#19967,1.);
#5426=VECTOR('',#19968,1.);
#5427=VECTOR('',#19969,1.);
#5428=VECTOR('',#19972,1.);
#5429=VECTOR('',#19973,1.);
#5430=VECTOR('',#19974,1.);
#5431=VECTOR('',#19977,1.);
#5432=VECTOR('',#19978,1.);
#5433=VECTOR('',#19979,1.);
#5434=VECTOR('',#19982,1.);
#5435=VECTOR('',#19983,1.);
#5436=VECTOR('',#19984,1.);
#5437=VECTOR('',#19987,1.);
#5438=VECTOR('',#19988,1.);
#5439=VECTOR('',#19989,1.);
#5440=VECTOR('',#19992,1.);
#5441=VECTOR('',#19993,1.);
#5442=VECTOR('',#20010,0.475);
#5443=VECTOR('',#20015,0.5);
#5444=VECTOR('',#20020,0.485);
#5445=VECTOR('',#20029,0.31);
#5446=VECTOR('',#20032,0.3);
#6384=CIRCLE('',#17402,0.2942);
#6385=CIRCLE('',#17404,0.45);
#6386=CIRCLE('',#17406,0.5);
#6387=CIRCLE('',#17408,0.5);
#6388=CIRCLE('',#17410,0.47);
#6389=CIRCLE('',#17412,0.32);
#6390=CIRCLE('',#17414,0.2942);
#7240=VERTEX_POINT('',#24116);
#7241=VERTEX_POINT('',#24117);
#7242=VERTEX_POINT('',#24119);
#7243=VERTEX_POINT('',#24121);
#7244=VERTEX_POINT('',#24125);
#7245=VERTEX_POINT('',#24127);
#7246=VERTEX_POINT('',#24131);
#7247=VERTEX_POINT('',#24133);
#7248=VERTEX_POINT('',#24137);
#7249=VERTEX_POINT('',#24139);
#7250=VERTEX_POINT('',#24143);
#7251=VERTEX_POINT('',#24145);
#7252=VERTEX_POINT('',#24154);
#7253=VERTEX_POINT('',#24157);
#7254=VERTEX_POINT('',#24160);
#7255=VERTEX_POINT('',#24164);
#7256=VERTEX_POINT('',#24168);
#7257=VERTEX_POINT('',#24172);
#7258=VERTEX_POINT('',#24175);
#8931=EDGE_CURVE('',#7240,#7241,#4400,.T.);
#8932=EDGE_CURVE('',#7241,#7242,#4401,.T.);
#8933=EDGE_CURVE('',#7242,#7243,#4402,.T.);
#8934=EDGE_CURVE('',#7240,#7243,#4403,.T.);
#8935=EDGE_CURVE('',#7241,#7244,#4404,.T.);
#8936=EDGE_CURVE('',#7244,#7245,#4405,.T.);
#8937=EDGE_CURVE('',#7245,#7242,#4406,.T.);
#8938=EDGE_CURVE('',#7244,#7246,#4407,.T.);
#8939=EDGE_CURVE('',#7246,#7247,#4408,.T.);
#8940=EDGE_CURVE('',#7247,#7245,#4409,.T.);
#8941=EDGE_CURVE('',#7246,#7248,#4410,.T.);
#8942=EDGE_CURVE('',#7248,#7249,#4411,.T.);
#8943=EDGE_CURVE('',#7249,#7247,#4412,.T.);
#8944=EDGE_CURVE('',#7248,#7250,#4413,.T.);
#8945=EDGE_CURVE('',#7250,#7251,#4414,.T.);
#8946=EDGE_CURVE('',#7251,#7249,#4415,.T.);
#8947=EDGE_CURVE('',#7250,#7240,#4416,.T.);
#8948=EDGE_CURVE('',#7243,#7251,#4417,.T.);
#8949=EDGE_CURVE('',#7252,#7252,#6384,.T.);
#8950=EDGE_CURVE('',#7253,#7253,#6385,.T.);
#8951=EDGE_CURVE('',#7254,#7254,#6386,.T.);
#8952=EDGE_CURVE('',#7254,#7253,#4418,.T.);
#8953=EDGE_CURVE('',#7255,#7255,#6387,.T.);
#8954=EDGE_CURVE('',#7255,#7254,#4419,.T.);
#8955=EDGE_CURVE('',#7256,#7256,#6388,.T.);
#8956=EDGE_CURVE('',#7256,#7255,#4420,.T.);
#8957=EDGE_CURVE('',#7257,#7257,#6389,.T.);
#8958=EDGE_CURVE('',#7258,#7258,#6390,.F.);
#8959=EDGE_CURVE('',#7258,#7257,#4421,.T.);
#8960=EDGE_CURVE('',#7252,#7258,#4422,.T.);
#11755=ORIENTED_EDGE('',*,*,#8931,.T.);
#11756=ORIENTED_EDGE('',*,*,#8932,.T.);
#11757=ORIENTED_EDGE('',*,*,#8933,.T.);
#11758=ORIENTED_EDGE('',*,*,#8934,.F.);
#11759=ORIENTED_EDGE('',*,*,#8935,.T.);
#11760=ORIENTED_EDGE('',*,*,#8936,.T.);
#11761=ORIENTED_EDGE('',*,*,#8937,.T.);
#11762=ORIENTED_EDGE('',*,*,#8932,.F.);
#11763=ORIENTED_EDGE('',*,*,#8938,.T.);
#11764=ORIENTED_EDGE('',*,*,#8939,.T.);
#11765=ORIENTED_EDGE('',*,*,#8940,.T.);
#11766=ORIENTED_EDGE('',*,*,#8936,.F.);
#11767=ORIENTED_EDGE('',*,*,#8941,.T.);
#11768=ORIENTED_EDGE('',*,*,#8942,.T.);
#11769=ORIENTED_EDGE('',*,*,#8943,.T.);
#11770=ORIENTED_EDGE('',*,*,#8939,.F.);
#11771=ORIENTED_EDGE('',*,*,#8944,.T.);
#11772=ORIENTED_EDGE('',*,*,#8945,.T.);
#11773=ORIENTED_EDGE('',*,*,#8946,.T.);
#11774=ORIENTED_EDGE('',*,*,#8942,.F.);
#11775=ORIENTED_EDGE('',*,*,#8947,.T.);
#11776=ORIENTED_EDGE('',*,*,#8934,.T.);
#11777=ORIENTED_EDGE('',*,*,#8948,.T.);
#11778=ORIENTED_EDGE('',*,*,#8945,.F.);
#11779=ORIENTED_EDGE('',*,*,#8947,.F.);
#11780=ORIENTED_EDGE('',*,*,#8944,.F.);
#11781=ORIENTED_EDGE('',*,*,#8941,.F.);
#11782=ORIENTED_EDGE('',*,*,#8938,.F.);
#11783=ORIENTED_EDGE('',*,*,#8935,.F.);
#11784=ORIENTED_EDGE('',*,*,#8931,.F.);
#11785=ORIENTED_EDGE('',*,*,#8948,.F.);
#11786=ORIENTED_EDGE('',*,*,#8933,.F.);
#11787=ORIENTED_EDGE('',*,*,#8937,.F.);
#11788=ORIENTED_EDGE('',*,*,#8940,.F.);
#11789=ORIENTED_EDGE('',*,*,#8943,.F.);
#11790=ORIENTED_EDGE('',*,*,#8946,.F.);
#11791=ORIENTED_EDGE('',*,*,#8949,.F.);
#11792=ORIENTED_EDGE('',*,*,#8950,.F.);
#11793=ORIENTED_EDGE('',*,*,#8951,.F.);
#11794=ORIENTED_EDGE('',*,*,#8952,.T.);
#11795=ORIENTED_EDGE('',*,*,#8950,.T.);
#11796=ORIENTED_EDGE('',*,*,#8952,.F.);
#11797=ORIENTED_EDGE('',*,*,#8953,.F.);
#11798=ORIENTED_EDGE('',*,*,#8954,.T.);
#11799=ORIENTED_EDGE('',*,*,#8951,.T.);
#11800=ORIENTED_EDGE('',*,*,#8954,.F.);
#11801=ORIENTED_EDGE('',*,*,#8955,.F.);
#11802=ORIENTED_EDGE('',*,*,#8956,.T.);
#11803=ORIENTED_EDGE('',*,*,#8953,.T.);
#11804=ORIENTED_EDGE('',*,*,#8956,.F.);
#11805=ORIENTED_EDGE('',*,*,#8955,.T.);
#11806=ORIENTED_EDGE('',*,*,#8957,.F.);
#11807=ORIENTED_EDGE('',*,*,#8958,.F.);
#11808=ORIENTED_EDGE('',*,*,#8959,.T.);
#11809=ORIENTED_EDGE('',*,*,#8957,.T.);
#11810=ORIENTED_EDGE('',*,*,#8959,.F.);
#11811=ORIENTED_EDGE('',*,*,#8949,.T.);
#11812=ORIENTED_EDGE('',*,*,#8960,.T.);
#11813=ORIENTED_EDGE('',*,*,#8958,.T.);
#11814=ORIENTED_EDGE('',*,*,#8960,.F.);
#15047=CYLINDRICAL_SURFACE('',#17407,0.5);
#15048=CYLINDRICAL_SURFACE('',#17415,0.2942);
#15491=ADVANCED_FACE('',(#2284),#1744,.F.);
#15492=ADVANCED_FACE('',(#2285),#1745,.F.);
#15493=ADVANCED_FACE('',(#2286),#1746,.F.);
#15494=ADVANCED_FACE('',(#2287),#1747,.F.);
#15495=ADVANCED_FACE('',(#2288),#1748,.F.);
#15496=ADVANCED_FACE('',(#2289),#1749,.F.);
#15497=ADVANCED_FACE('',(#2290),#1750,.F.);
#15498=ADVANCED_FACE('',(#2291),#1751,.F.);
#15499=ADVANCED_FACE('',(#2292),#1752,.F.);
#15500=ADVANCED_FACE('',(#2293),#1753,.T.);
#15501=ADVANCED_FACE('',(#2294),#1101,.T.);
#15502=ADVANCED_FACE('',(#2295),#15047,.T.);
#15503=ADVANCED_FACE('',(#2296),#1102,.T.);
#15504=ADVANCED_FACE('',(#2297,#1518),#1754,.T.);
#15505=ADVANCED_FACE('',(#2298),#1103,.T.);
#15506=ADVANCED_FACE('',(#2299),#15048,.T.);
#16138=CLOSED_SHELL('',(#15491,#15492,#15493,#15494,#15495,#15496,#15497,
#15498));
#16139=CLOSED_SHELL('',(#15499,#15500,#15501,#15502,#15503,#15504,#15505,
#15506));
#17392=AXIS2_PLACEMENT_3D('',#24114,#19962,#19963);
#17393=AXIS2_PLACEMENT_3D('',#24115,#19964,#19965);
#17394=AXIS2_PLACEMENT_3D('',#24124,#19970,#19971);
#17395=AXIS2_PLACEMENT_3D('',#24130,#19975,#19976);
#17396=AXIS2_PLACEMENT_3D('',#24136,#19980,#19981);
#17397=AXIS2_PLACEMENT_3D('',#24142,#19985,#19986);
#17398=AXIS2_PLACEMENT_3D('',#24148,#19990,#19991);
#17399=AXIS2_PLACEMENT_3D('',#24151,#19994,#19995);
#17400=AXIS2_PLACEMENT_3D('',#24152,#19996,#19997);
#17401=AXIS2_PLACEMENT_3D('',#24153,#19998,#19999);
#17402=AXIS2_PLACEMENT_3D('',#24155,#20000,#20001);
#17403=AXIS2_PLACEMENT_3D('',#24156,#20002,#20003);
#17404=AXIS2_PLACEMENT_3D('',#24158,#20004,#20005);
#17405=AXIS2_PLACEMENT_3D('',#24159,#20006,#20007);
#17406=AXIS2_PLACEMENT_3D('',#24161,#20008,#20009);
#17407=AXIS2_PLACEMENT_3D('',#24163,#20011,#20012);
#17408=AXIS2_PLACEMENT_3D('',#24165,#20013,#20014);
#17409=AXIS2_PLACEMENT_3D('',#24167,#20016,#20017);
#17410=AXIS2_PLACEMENT_3D('',#24169,#20018,#20019);
#17411=AXIS2_PLACEMENT_3D('',#24171,#20021,#20022);
#17412=AXIS2_PLACEMENT_3D('',#24173,#20023,#20024);
#17413=AXIS2_PLACEMENT_3D('',#24174,#20025,#20026);
#17414=AXIS2_PLACEMENT_3D('',#24176,#20027,#20028);
#17415=AXIS2_PLACEMENT_3D('',#24178,#20030,#20031);
#19962=DIRECTION('axis',(0.,0.,1.));
#19963=DIRECTION('refdir',(1.,0.,0.));
#19964=DIRECTION('center_axis',(0.866025403784439,0.,-0.5));
#19965=DIRECTION('ref_axis',(0.5,0.,0.866025403784439));
#19966=DIRECTION('',(-0.5,0.,-0.866025403784439));
#19967=DIRECTION('',(0.,-1.,0.));
#19968=DIRECTION('',(0.5,0.,0.866025403784439));
#19969=DIRECTION('',(0.,-1.,0.));
#19970=DIRECTION('center_axis',(1.92296268638356E-16,0.,-1.));
#19971=DIRECTION('ref_axis',(1.,0.,1.92296268638356E-16));
#19972=DIRECTION('',(-1.,0.,-1.92296268638356E-16));
#19973=DIRECTION('',(0.,-1.,0.));
#19974=DIRECTION('',(1.,0.,1.92296268638356E-16));
#19975=DIRECTION('center_axis',(-0.866025403784439,0.,-0.5));
#19976=DIRECTION('ref_axis',(0.5,0.,-0.866025403784439));
#19977=DIRECTION('',(-0.5,0.,0.866025403784438));
#19978=DIRECTION('',(0.,-1.,0.));
#19979=DIRECTION('',(0.5,0.,-0.866025403784438));
#19980=DIRECTION('center_axis',(-0.866025403784439,0.,0.5));
#19981=DIRECTION('ref_axis',(-0.5,0.,-0.866025403784439));
#19982=DIRECTION('',(0.5,0.,0.866025403784439));
#19983=DIRECTION('',(0.,-1.,0.));
#19984=DIRECTION('',(-0.5,0.,-0.866025403784439));
#19985=DIRECTION('center_axis',(-1.92296268638356E-16,0.,1.));
#19986=DIRECTION('ref_axis',(-1.,0.,-1.92296268638356E-16));
#19987=DIRECTION('',(1.,0.,1.92296268638356E-16));
#19988=DIRECTION('',(0.,-1.,0.));
#19989=DIRECTION('',(-1.,0.,-1.92296268638356E-16));
#19990=DIRECTION('center_axis',(0.866025403784439,0.,0.5));
#19991=DIRECTION('ref_axis',(-0.5,0.,0.866025403784439));
#19992=DIRECTION('',(0.5,0.,-0.866025403784439));
#19993=DIRECTION('',(-0.5,0.,0.866025403784439));
#19994=DIRECTION('center_axis',(0.,1.,0.));
#19995=DIRECTION('ref_axis',(1.,0.,0.));
#19996=DIRECTION('center_axis',(0.,-1.,0.));
#19997=DIRECTION('ref_axis',(0.,0.,-1.));
#19998=DIRECTION('center_axis',(0.,1.,0.));
#19999=DIRECTION('ref_axis',(1.,0.,0.));
#20000=DIRECTION('center_axis',(0.,1.,0.));
#20001=DIRECTION('ref_axis',(1.,0.,0.));
#20002=DIRECTION('center_axis',(0.,1.,0.));
#20003=DIRECTION('ref_axis',(0.,0.,1.));
#20004=DIRECTION('center_axis',(0.,-1.,0.));
#20005=DIRECTION('ref_axis',(1.,0.,0.));
#20006=DIRECTION('center_axis',(0.,-1.,0.));
#20007=DIRECTION('ref_axis',(1.,0.,0.));
#20008=DIRECTION('center_axis',(0.,-1.,0.));
#20009=DIRECTION('ref_axis',(1.,0.,0.));
#20010=DIRECTION('',(0.707106781186548,0.707106781186547,8.65956056235494E-17));
#20011=DIRECTION('center_axis',(0.,-1.,0.));
#20012=DIRECTION('ref_axis',(1.,0.,0.));
#20013=DIRECTION('center_axis',(0.,-1.,0.));
#20014=DIRECTION('ref_axis',(1.,0.,0.));
#20015=DIRECTION('',(0.,1.,0.));
#20016=DIRECTION('center_axis',(0.,1.,0.));
#20017=DIRECTION('ref_axis',(1.,0.,0.));
#20018=DIRECTION('center_axis',(0.,-1.,0.));
#20019=DIRECTION('ref_axis',(1.,0.,0.));
#20020=DIRECTION('',(-0.707106781186547,0.707106781186548,-8.65956056235493E-17));
#20021=DIRECTION('center_axis',(0.,-1.,0.));
#20022=DIRECTION('ref_axis',(0.,0.,-1.));
#20023=DIRECTION('center_axis',(0.,-1.,0.));
#20024=DIRECTION('ref_axis',(1.,0.,0.));
#20025=DIRECTION('center_axis',(0.,1.,0.));
#20026=DIRECTION('ref_axis',(1.,0.,0.));
#20027=DIRECTION('center_axis',(0.,1.,0.));
#20028=DIRECTION('ref_axis',(1.,0.,0.));
#20029=DIRECTION('',(-0.447213595499958,0.894427190999916,-5.47678698264203E-17));
#20030=DIRECTION('center_axis',(0.,-1.,0.));
#20031=DIRECTION('ref_axis',(1.,0.,0.));
#20032=DIRECTION('',(0.,1.,0.));
#24114=CARTESIAN_POINT('',(0.,0.,0.));
#24115=CARTESIAN_POINT('Origin',(0.144337567297406,-0.6,-0.25));
#24116=CARTESIAN_POINT('',(0.288675134594813,-0.6,0.));
#24117=CARTESIAN_POINT('',(0.144337567297406,-0.6,-0.25));
#24118=CARTESIAN_POINT('',(0.288675134594813,-0.6,0.));
#24119=CARTESIAN_POINT('',(0.144337567297406,-0.96,-0.25));
#24120=CARTESIAN_POINT('',(0.144337567297406,-0.6,-0.25));
#24121=CARTESIAN_POINT('',(0.288675134594813,-0.96,0.));
#24122=CARTESIAN_POINT('',(0.288675134594813,-0.96,0.));
#24123=CARTESIAN_POINT('',(0.288675134594813,-0.6,0.));
#24124=CARTESIAN_POINT('Origin',(-0.144337567297406,-0.6,-0.25));
#24125=CARTESIAN_POINT('',(-0.144337567297406,-0.6,-0.25));
#24126=CARTESIAN_POINT('',(0.144337567297406,-0.6,-0.25));
#24127=CARTESIAN_POINT('',(-0.144337567297406,-0.96,-0.25));
#24128=CARTESIAN_POINT('',(-0.144337567297406,-0.6,-0.25));
#24129=CARTESIAN_POINT('',(0.144337567297406,-0.96,-0.25));
#24130=CARTESIAN_POINT('Origin',(-0.288675134594813,-0.6,-8.32667268468867E-17));
#24131=CARTESIAN_POINT('',(-0.288675134594813,-0.6,-3.53525079574969E-17));
#24132=CARTESIAN_POINT('',(-0.144337567297406,-0.6,-0.25));
#24133=CARTESIAN_POINT('',(-0.288675134594813,-0.96,-5.55111512312578E-17));
#24134=CARTESIAN_POINT('',(-0.288675134594813,-0.6,-3.53525079574969E-17));
#24135=CARTESIAN_POINT('',(-0.144337567297406,-0.96,-0.25));
#24136=CARTESIAN_POINT('Origin',(-0.144337567297407,-0.6,0.25));
#24137=CARTESIAN_POINT('',(-0.144337567297407,-0.6,0.25));
#24138=CARTESIAN_POINT('',(-0.288675134594813,-0.6,-3.53525079574969E-17));
#24139=CARTESIAN_POINT('',(-0.144337567297407,-0.96,0.25));
#24140=CARTESIAN_POINT('',(-0.144337567297407,-0.6,0.25));
#24141=CARTESIAN_POINT('',(-0.288675134594813,-0.96,-3.53525079574969E-17));
#24142=CARTESIAN_POINT('Origin',(0.144337567297406,-0.6,0.25));
#24143=CARTESIAN_POINT('',(0.144337567297406,-0.6,0.25));
#24144=CARTESIAN_POINT('',(-0.144337567297407,-0.6,0.25));
#24145=CARTESIAN_POINT('',(0.144337567297406,-0.96,0.25));
#24146=CARTESIAN_POINT('',(0.144337567297406,-0.6,0.25));
#24147=CARTESIAN_POINT('',(-0.144337567297407,-0.96,0.25));
#24148=CARTESIAN_POINT('Origin',(0.288675134594813,-0.6,0.));
#24149=CARTESIAN_POINT('',(0.144337567297406,-0.6,0.25));
#24150=CARTESIAN_POINT('',(0.144337567297406,-0.96,0.25));
#24151=CARTESIAN_POINT('Origin',(0.,-0.6,0.));
#24152=CARTESIAN_POINT('Origin',(0.,-0.96,0.));
#24153=CARTESIAN_POINT('Origin',(0.,-1.8,0.));
#24154=CARTESIAN_POINT('',(-0.2942,-1.8,3.60291088309151E-17));
#24155=CARTESIAN_POINT('Origin',(0.,-1.8,0.));
#24156=CARTESIAN_POINT('Origin',(0.45,0.6,0.));
#24157=CARTESIAN_POINT('',(-0.45,0.6,-5.51091059616309E-17));
#24158=CARTESIAN_POINT('Origin',(0.,0.6,0.));
#24159=CARTESIAN_POINT('Origin',(0.,0.575,0.));
#24160=CARTESIAN_POINT('',(-0.5,0.55,-6.12323399573677E-17));
#24161=CARTESIAN_POINT('Origin',(0.,0.55,0.));
#24162=CARTESIAN_POINT('',(-0.475,0.575,-5.81707229594993E-17));
#24163=CARTESIAN_POINT('Origin',(0.,0.29,0.));
#24164=CARTESIAN_POINT('',(-0.5,0.0299999999999998,-6.12323399573677E-17));
#24165=CARTESIAN_POINT('Origin',(0.,0.0299999999999998,0.));
#24166=CARTESIAN_POINT('',(-0.5,0.29,-6.12323399573677E-17));
#24167=CARTESIAN_POINT('Origin',(0.,0.0150000000000001,0.));
#24168=CARTESIAN_POINT('',(-0.47,7.11236625150491E-17,-5.75583995599256E-17));
#24169=CARTESIAN_POINT('Origin',(0.,0.,0.));
#24170=CARTESIAN_POINT('',(-0.485,0.0150000000000001,-5.93953697586466E-17));
#24171=CARTESIAN_POINT('Origin',(0.32,0.,0.));
#24172=CARTESIAN_POINT('',(-0.32,-6.93889390390723E-18,-3.91886975727153E-17));
#24173=CARTESIAN_POINT('Origin',(0.,0.,0.));
#24174=CARTESIAN_POINT('Origin',(0.,-0.02,0.));
#24175=CARTESIAN_POINT('',(-0.2942,-0.0515999999999999,3.60291088309151E-17));
#24176=CARTESIAN_POINT('Origin',(0.,-0.0515999999999999,0.));
#24177=CARTESIAN_POINT('',(-0.31,-0.02,-3.7964050773568E-17));
#24178=CARTESIAN_POINT('Origin',(0.,-1.24,0.));
#24179=CARTESIAN_POINT('',(-0.2942,-1.24,-3.60291088309151E-17));
#73257=UNCERTAINTY_MEASURE_WITH_UNIT(LENGTH_MEASURE(0.001),#73367,
'DISTANCE_ACCURACY_VALUE',
'Maximum model space distance between geometric entities at asserted c
onnectivities');
#73302=UNCERTAINTY_MEASURE_WITH_UNIT(LENGTH_MEASURE(0.001),#73367,
'DISTANCE_ACCURACY_VALUE',
'Maximum model space distance between geometric entities at asserted c
onnectivities');
#73321=(
GEOMETRIC_REPRESENTATION_CONTEXT(3)
GLOBAL_UNCERTAINTY_ASSIGNED_CONTEXT((#73257))
GLOBAL_UNIT_ASSIGNED_CONTEXT((#73367,#73369,#73370))
REPRESENTATION_CONTEXT('','3D')
);
#73366=(
GEOMETRIC_REPRESENTATION_CONTEXT(3)
GLOBAL_UNCERTAINTY_ASSIGNED_CONTEXT((#73302))
GLOBAL_UNIT_ASSIGNED_CONTEXT((#73367,#73369,#73370))
REPRESENTATION_CONTEXT('','3D')
);
#73367=(
LENGTH_UNIT()
NAMED_UNIT(*)
SI_UNIT(.CENTI.,.METRE.)
);
#73369=(
NAMED_UNIT(*)
PLANE_ANGLE_UNIT()
SI_UNIT($,.RADIAN.)
);
#73370=(
NAMED_UNIT(*)
SI_UNIT($,.STERADIAN.)
SOLID_ANGLE_UNIT()
);
#73389=SHAPE_DEFINITION_REPRESENTATION(#73452,#73625);
#73452=PRODUCT_DEFINITION_SHAPE('',$,#73689);
#73625=SHAPE_REPRESENTATION('',(#17392),#73321);
#73670=PRODUCT_DEFINITION_CONTEXT('part definition',#73861,'design');
#73689=PRODUCT_DEFINITION('M6x18 mounting screw','M6x18 mounting screw',
#73752,#73670);
#73752=PRODUCT_DEFINITION_FORMATION('',$,#73881);
#73861=APPLICATION_CONTEXT(
'Core Data for Automotive Mechanical Design Process');
#73862=PRODUCT_CONTEXT('part definition',#73861,'mechanical');
#73881=PRODUCT('M6x18 mounting screw','M6x18 mounting screw',
'M6x18 mounting screw',(#73862));
#73989=COLOUR_RGB('Black',0.12,0.14,0.17);
#73990=FILL_AREA_STYLE_COLOUR('',#73989);
#73991=FILL_AREA_STYLE('',(#73990));
#73992=SURFACE_STYLE_FILL_AREA(#73991);
#73993=SURFACE_SIDE_STYLE('',(#73992));
#73994=SURFACE_STYLE_USAGE(.BOTH.,#73993);
#73995=PRESENTATION_STYLE_ASSIGNMENT((#73994));
ENDSEC;
END-ISO-10303-21;
